ISO-10303-21;
HEADER;
/* Generated by software containing ST-Developer
 * from STEP Tools, Inc. (www.steptools.com) 
 */
/* OPTION: using custom renumber hook */

FILE_DESCRIPTION(
/* description */ ('STEP AP242 Edition 2', 'CAx-IF Rec.Pracs.---Representation and Presentation of Product Manufa
cturing Information (PMI)---4.0---2014-10-13', 'CAx-IF Rec.Pracs.---3D Tessellated Geometry---0.4---2014-09-14', '2;1', 'CAx-IF Rec.Pracs.---User Defined Attributes---1.5---2016-08-15'),
/* implementation_level */ '2;1');

FILE_NAME(
/* name */ 'Part 1__PD8594.step',
/* time_stamp */ '2026-10-07T00:00:55Z',
/* author */ (''),
/* organization */ (''),
/* preprocessor_version */ 'ST-DEVELOPER v20',
/* originating_system */ 'ONSHAPE BY PTC INC, 1.221',
/* authorisation */ '  ');

FILE_SCHEMA (('AP242_MANAGED_MODEL_BASED_3D_ENGINEERING_MIM_LF { 1 0 10303 442 3 1 4 }'));
ENDSEC;

DATA;
#121=SHAPE_REPRESENTATION_RELATIONSHIP('','',#4477,#132);
#132=ADVANCED_BREP_SHAPE_REPRESENTATION('',(#4453),#8540);
#223=CYLINDRICAL_SURFACE('',#4594,0.0075);
#224=CYLINDRICAL_SURFACE('',#4595,0.01);
#350=CIRCLE('',#4589,0.0075);
#351=CIRCLE('',#4590,0.01);
#352=CIRCLE('',#4592,0.0075);
#353=CIRCLE('',#4593,0.01);
#855=ORIENTED_EDGE('',*,*,#1947,.F.);
#856=ORIENTED_EDGE('',*,*,#1948,.T.);
#857=ORIENTED_EDGE('',*,*,#1949,.T.);
#858=ORIENTED_EDGE('',*,*,#1950,.F.);
#859=ORIENTED_EDGE('',*,*,#1947,.T.);
#860=ORIENTED_EDGE('',*,*,#1949,.F.);
#861=ORIENTED_EDGE('',*,*,#1948,.F.);
#862=ORIENTED_EDGE('',*,*,#1950,.T.);
#1947=EDGE_CURVE('',#2516,#2516,#350,.T.);
#1948=EDGE_CURVE('',#2517,#2517,#351,.T.);
#1949=EDGE_CURVE('',#2518,#2518,#352,.T.);
#1950=EDGE_CURVE('',#2519,#2519,#353,.T.);
#2516=VERTEX_POINT('',#6718);
#2517=VERTEX_POINT('',#6720);
#2518=VERTEX_POINT('',#6723);
#2519=VERTEX_POINT('',#6725);
#3282=EDGE_LOOP('',(#855));
#3283=EDGE_LOOP('',(#856));
#3284=EDGE_LOOP('',(#857));
#3285=EDGE_LOOP('',(#858));
#3286=EDGE_LOOP('',(#859));
#3287=EDGE_LOOP('',(#860));
#3288=EDGE_LOOP('',(#861));
#3289=EDGE_LOOP('',(#862));
#3659=FACE_BOUND('',#3282,.T.);
#3660=FACE_BOUND('',#3283,.T.);
#3661=FACE_BOUND('',#3284,.T.);
#3662=FACE_BOUND('',#3285,.T.);
#3663=FACE_BOUND('',#3286,.T.);
#3664=FACE_BOUND('',#3287,.T.);
#3665=FACE_BOUND('',#3288,.T.);
#3666=FACE_BOUND('',#3289,.T.);
#3972=PLANE('',#4588);
#3973=PLANE('',#4591);
#4091=ADVANCED_FACE('',(#3659,#3660),#3972,.T.);
#4092=ADVANCED_FACE('',(#3661,#3662),#3973,.F.);
#4093=ADVANCED_FACE('',(#3663,#3664),#223,.F.);
#4094=ADVANCED_FACE('',(#3665,#3666),#224,.T.);
#4327=CLOSED_SHELL('',(#4091,#4092,#4093,#4094));
#4338=STYLED_ITEM('',(#4349),#4453);
#4349=PRESENTATION_STYLE_ASSIGNMENT((#4365));
#4365=SURFACE_STYLE_USAGE(.BOTH.,#4381);
#4381=SURFACE_SIDE_STYLE('',(#4397));
#4397=SURFACE_STYLE_FILL_AREA(#4413);
#4413=FILL_AREA_STYLE('',(#4429));
#4429=FILL_AREA_STYLE_COLOUR('',#4442);
#4442=COLOUR_RGB('', 0.31764706, 0.68627451, 0.89019608);
#4453=MANIFOLD_SOLID_BREP('Part 1',#4327);
#4465=SHAPE_DEFINITION_REPRESENTATION(#8573,#4477);
#4477=SHAPE_REPRESENTATION('Part 1',(#4484),#8540);
#4484=AXIS2_PLACEMENT_3D('',#6402,#5064,#5065);
#4588=AXIS2_PLACEMENT_3D('',#6716,#5292,#5293);
#4589=AXIS2_PLACEMENT_3D('',#6717,#5294,#5295);
#4590=AXIS2_PLACEMENT_3D('',#6719,#5296,#5297);
#4591=AXIS2_PLACEMENT_3D('',#6721,#5298,#5299);
#4592=AXIS2_PLACEMENT_3D('',#6722,#5300,#5301);
#4593=AXIS2_PLACEMENT_3D('',#6724,#5302,#5303);
#4594=AXIS2_PLACEMENT_3D('',#6726,#5304,#5305);
#4595=AXIS2_PLACEMENT_3D('',#6727,#5306,#5307);
#5064=DIRECTION('',(0.,0.,1.));
#5065=DIRECTION('',(1.,0.,0.));
#5292=DIRECTION('',(0.,0.,1.));
#5293=DIRECTION('',(1.,0.,0.));
#5294=DIRECTION('',(0.,0.,1.));
#5295=DIRECTION('',(1.,0.,0.));
#5296=DIRECTION('',(0.,0.,1.));
#5297=DIRECTION('',(1.,0.,0.));
#5298=DIRECTION('',(0.,0.,1.));
#5299=DIRECTION('',(1.,0.,0.));
#5300=DIRECTION('',(0.,0.,1.));
#5301=DIRECTION('',(1.,0.,0.));
#5302=DIRECTION('',(0.,0.,1.));
#5303=DIRECTION('',(1.,0.,0.));
#5304=DIRECTION('',(0.,0.,-1.));
#5305=DIRECTION('',(-1.,0.,0.));
#5306=DIRECTION('',(0.,0.,1.));
#5307=DIRECTION('',(1.,0.,0.));
#6402=CARTESIAN_POINT('',(0.,0.,0.));
#6716=CARTESIAN_POINT('',(0.,0.,0.034));
#6717=CARTESIAN_POINT('',(0.,0.,0.034));
#6718=CARTESIAN_POINT('',(0.0075,0.,0.034));
#6719=CARTESIAN_POINT('',(0.,6.12323399573677E-19,0.034));
#6720=CARTESIAN_POINT('',(0.01,6.12323399573677E-19,0.034));
#6721=CARTESIAN_POINT('',(0.,0.,-0.034));
#6722=CARTESIAN_POINT('',(0.,0.,-0.034));
#6723=CARTESIAN_POINT('',(0.0075,0.,-0.034));
#6724=CARTESIAN_POINT('',(0.,6.12323399573677E-19,-0.034));
#6725=CARTESIAN_POINT('',(0.01,6.12323399573677E-19,-0.034));
#6726=CARTESIAN_POINT('',(0.,0.,0.034));
#6727=CARTESIAN_POINT('',(0.,6.12323399573677E-19,-0.0747896763833597));
#8534=MECHANICAL_DESIGN_GEOMETRIC_PRESENTATION_REPRESENTATION('',(#4338),#8535);
#8535=(
GEOMETRIC_REPRESENTATION_CONTEXT(3)
GLOBAL_UNCERTAINTY_ASSIGNED_CONTEXT((#8547))
GLOBAL_UNIT_ASSIGNED_CONTEXT((#8561,#8560,#8559))
REPRESENTATION_CONTEXT('MAS-680','TOP_LEVEL_ASSEMBLY_PART')
);
#8540=(
GEOMETRIC_REPRESENTATION_CONTEXT(3)
GLOBAL_UNCERTAINTY_ASSIGNED_CONTEXT((#8552))
GLOBAL_UNIT_ASSIGNED_CONTEXT((#8561,#8560,#8559))
REPRESENTATION_CONTEXT('Part 1','COMPONENT_PART')
);
#8547=UNCERTAINTY_MEASURE_WITH_UNIT(LENGTH_MEASURE(1.E-8),#8561,
'DISTANCE_ACCURACY_VALUE','Maximum Tolerance applied to model');
#8552=UNCERTAINTY_MEASURE_WITH_UNIT(LENGTH_MEASURE(1.E-8),#8561,
'DISTANCE_ACCURACY_VALUE','Maximum Tolerance applied to model');
#8559=(
NAMED_UNIT(*)
SI_UNIT($,.STERADIAN.)
SOLID_ANGLE_UNIT()
);
#8560=(
NAMED_UNIT(*)
PLANE_ANGLE_UNIT()
SI_UNIT($,.RADIAN.)
);
#8561=(
LENGTH_UNIT()
NAMED_UNIT(*)
SI_UNIT($,.METRE.)
);
#8573=PRODUCT_DEFINITION_SHAPE('','',#8594);
#8594=PRODUCT_DEFINITION('','',#8618,#8606);
#8606=PRODUCT_DEFINITION_CONTEXT('',#8674,'design');
#8618=PRODUCT_DEFINITION_FORMATION_WITH_SPECIFIED_SOURCE('','',#8642,
 .NOT_KNOWN.);
#8642=PRODUCT('Part 1','Part 1','Part 1',(#8666));
#8666=PRODUCT_CONTEXT('',#8674,'mechanical');
#8674=APPLICATION_CONTEXT('managed model based 3d engineering');
ENDSEC;
END-ISO-10303-21;
